ISO-10303-21;
HEADER;
FILE_DESCRIPTION (('STEP AP214'),
    '1' );
FILE_NAME ('hex bolt gradeab_iso_ISO 4014 - M10 x 45 x 26-N.step',
    '2026-10-06T07:34:29',
    ( '' ),
    ( '' ),
    'SwSTEP 2.0',
    'SolidWorks 2025',
    '' );
FILE_SCHEMA (( 'AUTOMOTIVE_DESIGN' ));
ENDSEC;

DATA;
#3=CIRCLE ( 'NONE', #12613, 8.000000000000028422 ) ;
#44=EDGE_CURVE ( 'NONE', #6556, #10266, #3803, .T. ) ;
#50=VERTEX_POINT ( 'NONE', #13007 ) ;
#104=ORIENTED_EDGE ( 'NONE', *, *, #13012, .T. ) ;
#105=ORIENTED_EDGE ( 'NONE', *, *, #5952, .T. ) ;
#110=CARTESIAN_POINT ( 'NONE',  ( 5.799999999999999822, -4.618802153517037823, -7.999999999999979572 ) ) ;
#113=DIRECTION ( 'NONE',  ( 1.000000000000000000, 0.000000000000000000, 0.000000000000000000 ) ) ;
#155=ORIENTED_EDGE ( 'NONE', *, *, #7793, .T. ) ;
#183=DIRECTION ( 'NONE',  ( 1.000000000000000000, 0.000000000000000000, 0.000000000000000000 ) ) ;
#193=DIRECTION ( 'NONE',  ( 0.000000000000000000, 0.000000000000000000, -1.000000000000000000 ) ) ;
#207=VERTEX_POINT ( 'NONE', #5995 ) ;
#223=AXIS2_PLACEMENT_3D ( 'NONE', #7936, #9115, #2067 ) ;
#243=MANIFOLD_SOLID_BREP ( 'HeadFillet', #9878 ) ;
#265=AXIS2_PLACEMENT_3D ( 'NONE', #2568, #9839, #9679 ) ;
#282=CARTESIAN_POINT ( 'NONE',  ( 0.7145311798163189732, 4.618802153516981868, 8.000000000000007105 ) ) ;
#314=ORIENTED_EDGE ( 'NONE', *, *, #44, .F. ) ;
#318=EDGE_CURVE ( 'NONE', #326, #5664, #13476, .T. ) ;
#326=VERTEX_POINT ( 'NONE', #14806 ) ;
#338=EDGE_CURVE ( 'NONE', #908, #14204, #13896, .T. ) ;
#373=AXIS2_PLACEMENT_3D ( 'NONE', #13663, #6109, #10928 ) ;
#379=VERTEX_POINT ( 'NONE', #14473 ) ;
#381=PRODUCT_CONTEXT ( 'NONE', #8388, 'mechanical' ) ;
#415=ADVANCED_FACE ( 'NONE', ( #12037 ), #9890, .T. ) ;
#420=CYLINDRICAL_SURFACE ( 'NONE', #12715, 5.000000000000017764 ) ;
#536=ORIENTED_EDGE ( 'NONE', *, *, #7965, .T. ) ;
#593=B_SPLINE_CURVE_WITH_KNOTS ( 'NONE', 3,
 ( #14279, #11773, #13093, #6006, #2212, #5766 ),
 .UNSPECIFIED., .F., .F.,
 ( 4, 2, 4 ),
 ( 0.008690415895085797093, 0.01102883710845593487, 0.01336725832182607265 ),
 .UNSPECIFIED. ) ;
#624=EDGE_CURVE ( 'NONE', #8392, #8751, #593, .T. ) ;
#626=FACE_OUTER_BOUND ( 'NONE', #9253, .T. ) ;
#637=CARTESIAN_POINT ( 'NONE',  ( 0.7145311798163155315, -4.618802153516981868, 8.000000000000007105 ) ) ;
#639=DIRECTION ( 'NONE',  ( 0.000000000000000000, 0.000000000000000000, -1.000000000000000000 ) ) ;
#643=CIRCLE ( 'NONE', #1402, 5.400000000000019007 ) ;
#743=DIRECTION ( 'NONE',  ( -1.000000000000000000, 0.000000000000000000, 0.000000000000000000 ) ) ;
#770=CARTESIAN_POINT ( 'NONE',  ( 0.08224679563972137064, -7.710515798486379246, -2.644994884459106466 ) ) ;
#775=CIRCLE ( 'NONE', #5318, 8.000000000000028422 ) ;
#784=CIRCLE ( 'NONE', #4837, 8.000000000000028422 ) ;
#791=EDGE_CURVE ( 'NONE', #2861, #14616, #12302, .T. ) ;
#826=CARTESIAN_POINT ( 'NONE',  ( 0.3173508448886544486, 8.480771745766400471, 1.310872448937999035 ) ) ;
#829=FACE_OUTER_BOUND ( 'NONE', #8158, .T. ) ;
#874=CARTESIAN_POINT ( 'NONE',  ( 51.39999999999999858, 0.000000000000000000, 0.000000000000000000 ) ) ;
#905=PLANE ( 'NONE',  #8362 ) ;
#908=VERTEX_POINT ( 'NONE', #2036 ) ;
#930=CARTESIAN_POINT ( 'NONE',  ( 0.000000000000000000, -6.928203230275514990, 4.000000000000058620 ) ) ;
#950=VECTOR ( 'NONE', #5040, 1000.000000000000000 ) ;
#967=EDGE_CURVE ( 'NONE', #50, #4287, #14667, .T. ) ;
#969=CARTESIAN_POINT ( 'NONE',  ( 0.3167204509598372519, 5.377136764700148674, 6.686525924292801903 ) ) ;
#995=DIRECTION ( 'NONE',  ( 0.000000000000000000, 0.000000000000000000, 1.000000000000000000 ) ) ;
#1012=CARTESIAN_POINT ( 'NONE',  ( -6.657678965418798693E-16, -7.321656987762860780, 3.318518101603048276 ) ) ;
#1028=EDGE_CURVE ( 'NONE', #2448, #379, #6375, .T. ) ;
#1031=EDGE_LOOP ( 'NONE', ( #14134, #3474, #14069, #6884 ) ) ;
#1039=LINE ( 'NONE', #8549, #12659 ) ;
#1043=CARTESIAN_POINT ( 'NONE',  ( 50.57199999999998852, 0.000000000000000000, 0.000000000000000000 ) ) ;
#1064=EDGE_LOOP ( 'NONE', ( #7124, #5619, #4807, #15346, #2670, #14276 ) ) ;
#1074=CARTESIAN_POINT ( 'NONE',  ( 0.7145311798163189732, 4.618802153516981868, -7.999999999999979572 ) ) ;
#1082=CARTESIAN_POINT ( 'NONE',  ( 0.000000000000000000, 0.000000000000000000, 0.000000000000000000 ) ) ;
#1109=LINE ( 'NONE', #3563, #4063 ) ;
#1123=CARTESIAN_POINT ( 'NONE',  ( 51.39999999999999858, 0.000000000000000000, 4.172000000000013920 ) ) ;
#1131=CARTESIAN_POINT ( 'NONE',  ( 0.06809871960542698832, 6.146186931204399961, 5.354491962338134847 ) ) ;
#1141=B_SPLINE_CURVE_WITH_KNOTS ( 'NONE', 3,
 ( #9451, #1143, #4386, #9217, #6853, #826, #13051, #2254 ),
 .UNSPECIFIED., .F., .F.,
 ( 4, 2, 2, 4 ),
 ( 0.004673709593152155714, 0.005837709341827646871, 0.007001709090503138028, 0.009329708587854120341 ),
 .UNSPECIFIED. ) ;
#1143=CARTESIAN_POINT ( 'NONE',  ( -5.065680541054341600E-15, 7.124194613927618214, 3.660532965668821692 ) ) ;
#1146=AXIS2_PLACEMENT_3D ( 'NONE', #5074, #9818, #3958 ) ;
#1199=DIRECTION ( 'NONE',  ( 0.000000000000000000, 0.000000000000000000, 1.000000000000000000 ) ) ;
#1214=VERTEX_POINT ( 'NONE', #4076 ) ;
#1224=CARTESIAN_POINT ( 'NONE',  ( 0.4988340113715718505, 3.871605243926934392, -7.999999999999981348 ) ) ;
#1232=FACE_OUTER_BOUND ( 'NONE', #10027, .T. ) ;
#1250=ORIENTED_EDGE ( 'NONE', *, *, #13676, .T. ) ;
#1276=AXIS2_PLACEMENT_3D ( 'NONE', #2453, #14444, #8319 ) ;
#1311=EDGE_CURVE ( 'NONE', #1809, #4918, #8825, .T. ) ;
#1379=CARTESIAN_POINT ( 'NONE',  ( 4.007948148170534052E-15, 0.3912769056150322000, 8.000000000000007105 ) ) ;
#1402=AXIS2_PLACEMENT_3D ( 'NONE', #5598, #4400, #13879 ) ;
#1408=ORIENTED_EDGE ( 'NONE', *, *, #10370, .F. ) ;
#1422=EDGE_CURVE ( 'NONE', #207, #11026, #1141, .T. ) ;
#1452=CIRCLE ( 'NONE', #14308, 4.172000000000013920 ) ;
#1455=DIRECTION ( 'NONE',  ( -1.000000000000000000, 0.000000000000000000, 0.000000000000000000 ) ) ;
#1462=CARTESIAN_POINT ( 'NONE',  ( 0.000000000000000000, 0.000000000000000000, 0.000000000000000000 ) ) ;
#1464=ADVANCED_FACE ( 'NONE', ( #10714 ), #13058, .T. ) ;
#1468=B_SPLINE_CURVE_WITH_KNOTS ( 'NONE', 3,
 ( #4611, #14305, #969, #1131, #5799, #10777 ),
 .UNSPECIFIED., .F., .F.,
 ( 4, 2, 4 ),
 ( 2.380731630171312408E-07, 0.002336973833157586326, 0.004673709593152155714 ),
 .UNSPECIFIED. ) ;
#1505=EDGE_CURVE ( 'NONE', #15035, #2448, #4359, .T. ) ;
#1532=CARTESIAN_POINT ( 'NONE',  ( 6.399999999999999467, 4.618802153516981868, -7.999999999999979572 ) ) ;
#1536=ORIENTED_EDGE ( 'NONE', *, *, #12679, .F. ) ;
#1551=AXIS2_PLACEMENT_3D ( 'NONE', #15520, #15282, #4640 ) ;
#1559=DIRECTION ( 'NONE',  ( 0.000000000000000000, -0.5000000000000019984, -0.8660254037844375974 ) ) ;
#1566=PRODUCT_DEFINITION_CONTEXT ( 'detailed design', #10793, 'design' ) ;
#1621=CARTESIAN_POINT ( 'NONE',  ( 0.3167204509598230411, -5.377136764700228611, -6.686525924292699763 ) ) ;
#1624=AXIS2_PLACEMENT_3D ( 'NONE', #1082, #11907, #8594 ) ;
#1666=EDGE_LOOP ( 'NONE', ( #7048, #3166, #11016, #2259, #104, #12408 ) ) ;
#1688=CARTESIAN_POINT ( 'NONE',  ( 5.799999999999999822, 4.618802153516981868, 8.000000000000007105 ) ) ;
#1689=ORIENTED_EDGE ( 'NONE', *, *, #1311, .T. ) ;
#1699=FACE_OUTER_BOUND ( 'NONE', #1894, .T. ) ;
#1712=DIRECTION ( 'NONE',  ( 1.000000000000000000, 0.000000000000000000, 0.000000000000000000 ) ) ;
#1733=CARTESIAN_POINT ( 'NONE',  ( -1.820951430007294553E-14, 7.321656987762852786, -3.318518101602990988 ) ) ;
#1748=ORIENTED_EDGE ( 'NONE', *, *, #6543, .F. ) ;
#1757=DIRECTION ( 'NONE',  ( 0.000000000000000000, 0.000000000000000000, -1.000000000000000000 ) ) ;
#1780=VERTEX_POINT ( 'NONE', #7055 ) ;
#1809=VERTEX_POINT ( 'NONE', #11711 ) ;
#1831=CARTESIAN_POINT ( 'NONE',  ( 0.08224679563971951102, -6.145890662064638299, 5.355005115540925509 ) ) ;
#1836=VECTOR ( 'NONE', #7426, 999.9999999999997726 ) ;
#1847=AXIS2_PLACEMENT_3D ( 'NONE', #5513, #3933, #8755 ) ;
#1849=DIRECTION ( 'NONE',  ( -1.000000000000000000, 0.000000000000000000, 0.000000000000000000 ) ) ;
#1894=EDGE_LOOP ( 'NONE', ( #11736, #12320, #155 ) ) ;
#1982=CARTESIAN_POINT ( 'NONE',  ( 0.3173508448886587785, -5.375634714784612633, 6.689127551062028942 ) ) ;
#2000=CIRCLE ( 'NONE', #10341, 8.000000000000028422 ) ;
#2010=DIRECTION ( 'NONE',  ( 1.000000000000000000, 0.000000000000000000, 0.000000000000000000 ) ) ;
#2022=CARTESIAN_POINT ( 'NONE',  ( 0.7145311798163155315, -4.618802153516981868, 8.000000000000007105 ) ) ;
#2030=CARTESIAN_POINT ( 'NONE',  ( 50.57199999999998852, 6.123233995736767268E-16, -5.000000000000000000 ) ) ;
#2036=CARTESIAN_POINT ( 'NONE',  ( 51.39999999999999858, 0.000000000000000000, 4.172000000000013920 ) ) ;
#2046=FACE_OUTER_BOUND ( 'NONE', #7317, .T. ) ;
#2053=CARTESIAN_POINT ( 'NONE',  ( 6.800000000000000711, 0.000000000000000000, 0.000000000000000000 ) ) ;
#2067=DIRECTION ( 'NONE',  ( 0.000000000000000000, 0.000000000000000000, 1.000000000000000000 ) ) ;
#2069=B_SPLINE_CURVE_WITH_KNOTS ( 'NONE', 3,
 ( #10264, #5683, #11450, #770, #15056, #4246, #9008, #8150 ),
 .UNSPECIFIED., .F., .F.,
 ( 4, 2, 2, 4 ),
 ( 0.004673709593152115815, 0.005837709341827616513, 0.007001709090503118078, 0.009329708587854120341 ),
 .UNSPECIFIED. ) ;
#2087=DIRECTION ( 'NONE',  ( 0.000000000000000000, 0.000000000000000000, 1.000000000000000000 ) ) ;
#2142=VERTEX_POINT ( 'NONE', #11291 ) ;
#2174=EDGE_CURVE ( 'NONE', #11026, #379, #5846, .T. ) ;
#2192=FACE_OUTER_BOUND ( 'NONE', #1666, .T. ) ;
#2197=ORIENTED_EDGE ( 'NONE', *, *, #2206, .T. ) ;
#2206=EDGE_CURVE ( 'NONE', #326, #1809, #3, .T. ) ;
#2212=CARTESIAN_POINT ( 'NONE',  ( 4.030182763035961013E-15, -0.7818963812180698136, 8.000000000000007105 ) ) ;
#2247=CARTESIAN_POINT ( 'NONE',  ( 0.7145311798163189732, 4.618802153516981868, -7.999999999999979572 ) ) ;
#2254=CARTESIAN_POINT ( 'NONE',  ( 0.7145311798163258565, 9.237604307034018802, 0.000000000000000000 ) ) ;
#2259=ORIENTED_EDGE ( 'NONE', *, *, #13517, .F. ) ;
#2276=AXIS2_PLACEMENT_3D ( 'NONE', #3759, #7408, #3678 ) ;
#2316=CARTESIAN_POINT ( 'NONE',  ( 0.7145311798163189732, 4.618802153516981868, -7.999999999999979572 ) ) ;
#2317=ORIENTED_EDGE ( 'NONE', *, *, #4716, .T. ) ;
#2324=CARTESIAN_POINT ( 'NONE',  ( 5.799999999999999822, 0.000000000000000000, 0.000000000000000000 ) ) ;
#2331=EDGE_CURVE ( 'NONE', #4918, #326, #9246, .T. ) ;
#2337=CARTESIAN_POINT ( 'NONE',  ( 5.799999999999999822, -2.775557561562891351E-14, -8.000000000000007105 ) ) ;
#2351=DIRECTION ( 'NONE',  ( 1.000000000000000000, 0.000000000000000000, 0.000000000000000000 ) ) ;
#2369=CONICAL_SURFACE ( 'NONE', #11202, 8.000000000000028422, 1.047197551196600296 ) ;
#2405=CARTESIAN_POINT ( 'NONE',  ( 0.3173508448886365740, 5.375634714784594870, -6.689127551061989863 ) ) ;
#2408=DIRECTION ( 'NONE',  ( 1.000000000000000000, 0.000000000000000000, 0.000000000000000000 ) ) ;
#2425=DIRECTION ( 'NONE',  ( 0.000000000000000000, 0.000000000000000000, 1.000000000000000000 ) ) ;
#2438=SURFACE_SIDE_STYLE ('',( #7425 ) ) ;
#2448=VERTEX_POINT ( 'NONE', #15525 ) ;
#2453=CARTESIAN_POINT ( 'NONE',  ( 0.000000000000000000, 0.000000000000000000, 0.000000000000000000 ) ) ;
#2502=CIRCLE ( 'NONE', #13082, 8.000000000000028422 ) ;
#2560=CARTESIAN_POINT ( 'NONE',  ( 0.000000000000000000, 0.000000000000000000, 5.000000000000017764 ) ) ;
#2567=ORIENTED_EDGE ( 'NONE', *, *, #6390, .F. ) ;
#2568=CARTESIAN_POINT ( 'NONE',  ( 51.39999999999999858, 0.000000000000000000, 0.000000000000000000 ) ) ;
#2573=EDGE_CURVE ( 'NONE', #14639, #15035, #2678, .T. ) ;
#2599=FILL_AREA_STYLE_COLOUR ( '', #6383 ) ;
#2622=CIRCLE ( 'NONE', #12941, 0.4000000000000001887 ) ;
#2625=ORIENTED_EDGE ( 'NONE', *, *, #10969, .T. ) ;
#2646=ORIENTED_EDGE ( 'NONE', *, *, #1028, .T. ) ;
#2662=DIRECTION ( 'NONE',  ( 0.000000000000000000, 0.000000000000000000, -1.000000000000000000 ) ) ;
#2670=ORIENTED_EDGE ( 'NONE', *, *, #6962, .F. ) ;
#2678=LINE ( 'NONE', #2836, #14526 ) ;
#2685=ORIENTED_EDGE ( 'NONE', *, *, #6294, .T. ) ;
#2721=ORIENTED_EDGE ( 'NONE', *, *, #9924, .T. ) ;
#2734=CARTESIAN_POINT ( 'NONE',  ( 0.7145311798161593231, -4.618802153517259867, -7.999999999999979572 ) ) ;
#2788=PLANE ( 'NONE',  #3260 ) ;
#2829=ORIENTED_EDGE ( 'NONE', *, *, #2573, .F. ) ;
#2836=CARTESIAN_POINT ( 'NONE',  ( 6.399999999999999467, 4.618802153516981868, -7.999999999999979572 ) ) ;
#2861=VERTEX_POINT ( 'NONE', #110 ) ;
#2874=ORIENTED_EDGE ( 'NONE', *, *, #3740, .T. ) ;
#2883=DIRECTION ( 'NONE',  ( 1.000000000000000000, 0.000000000000000000, 0.000000000000000000 ) ) ;
#2931=DIRECTION ( 'NONE',  ( 1.000000000000000000, 0.000000000000000000, 0.000000000000000000 ) ) ;
#2935=CARTESIAN_POINT ( 'NONE',  ( 0.4964154566687820624, 8.859816792613631975, -0.6543471694412253958 ) ) ;
#3001=ORIENTED_EDGE ( 'NONE', *, *, #14701, .T. ) ;
#3014=CIRCLE ( 'NONE', #9074, 8.000000000000028422 ) ;
#3048=CARTESIAN_POINT ( 'NONE',  ( 0.000000000000000000, 0.000000000000000000, 0.000000000000000000 ) ) ;
#3052=CARTESIAN_POINT ( 'NONE',  ( 0.000000000000000000, 6.123233995736787976E-16, -5.000000000000017764 ) ) ;
#3073=EDGE_CURVE ( 'NONE', #5664, #6556, #9930, .T. ) ;
#3103=ORIENTED_EDGE ( 'NONE', *, *, #10488, .T. ) ;
#3104=CARTESIAN_POINT ( 'NONE',  ( 0.000000000000000000, 0.000000000000000000, 8.000000000000007105 ) ) ;
#3145=DIRECTION ( 'NONE',  ( 0.000000000000000000, -0.4999999999999996669, 0.8660254037844388186 ) ) ;
#3166=ORIENTED_EDGE ( 'NONE', *, *, #6294, .F. ) ;
#3203=CARTESIAN_POINT ( 'NONE',  ( 50.57199999999998852, 0.000000000000000000, 0.000000000000000000 ) ) ;
#3226=EDGE_LOOP ( 'NONE', ( #7677, #1250, #9326, #7247 ) ) ;
#3228=CARTESIAN_POINT ( 'NONE',  ( 5.799999999999999822, 7.999999999999979572, 0.000000000000000000 ) ) ;
#3229=ORIENTED_EDGE ( 'NONE', *, *, #6397, .T. ) ;
#3237=ADVANCED_FACE ( 'NONE', ( #9282 ), #8114, .T. ) ;
#3255=DIRECTION ( 'NONE',  ( 0.000000000000000000, 0.5000000000000019984, 0.8660254037844375974 ) ) ;
#3260=AXIS2_PLACEMENT_3D ( 'NONE', #8787, #7927, #7850 ) ;
#3325=DIRECTION ( 'NONE',  ( 0.000000000000000000, 0.5000000000000011102, -0.8660254037844380415 ) ) ;
#3337=EDGE_CURVE ( 'NONE', #10460, #207, #1468, .T. ) ;
#3368=PLANE ( 'NONE',  #11630 ) ;
#3387=SHAPE_REPRESENTATION ( 'hex bolt gradeab_iso_ISO 4014 - M10 x 45 x 26-N', ( #12337 ), #10810 ) ;
#3391=LINE ( 'NONE', #5837, #8620 ) ;
#3393=CARTESIAN_POINT ( 'NONE',  ( 0.000000000000000000, -6.928203230275514990, 4.000000000000058620 ) ) ;
#3474=ORIENTED_EDGE ( 'NONE', *, *, #4716, .F. ) ;
#3538=DIRECTION ( 'NONE',  ( 0.000000000000000000, 0.000000000000000000, -1.000000000000000000 ) ) ;
#3554=VERTEX_POINT ( 'NONE', #6676 ) ;
#3562=CARTESIAN_POINT ( 'NONE',  ( 5.799999999999999822, 9.237604307034018802, 0.000000000000000000 ) ) ;
#3563=CARTESIAN_POINT ( 'NONE',  ( 5.799999999999999822, 4.618802153516981868, 8.000000000000007105 ) ) ;
#3657=EDGE_LOOP ( 'NONE', ( #12916, #10360, #4408, #5195, #10618, #11788 ) ) ;
#3658=DIRECTION ( 'NONE',  ( -1.000000000000000000, 0.000000000000000000, 0.000000000000000000 ) ) ;
#3665=CARTESIAN_POINT ( 'NONE',  ( 0.08224679563969686247, 6.145890662064630305, -5.355005115540884653 ) ) ;
#3668=CARTESIAN_POINT ( 'NONE',  ( 0.000000000000000000, 0.000000000000000000, 0.000000000000000000 ) ) ;
#3678=DIRECTION ( 'NONE',  ( 0.000000000000000000, 0.000000000000000000, -1.000000000000000000 ) ) ;
#3729=CIRCLE ( 'NONE', #14557, 5.000000000000017764 ) ;
#3737=DIRECTION ( 'NONE',  ( -1.000000000000000000, 0.000000000000000000, 0.000000000000000000 ) ) ;
#3740=EDGE_CURVE ( 'NONE', #14616, #2142, #13555, .T. ) ;
#3759=CARTESIAN_POINT ( 'NONE',  ( 0.000000000000000000, 0.000000000000000000, 0.000000000000000000 ) ) ;
#3767=DIRECTION ( 'NONE',  ( 0.000000000000000000, 0.000000000000000000, -1.000000000000000000 ) ) ;
#3785=CARTESIAN_POINT ( 'NONE',  ( 5.799999999999999822, 0.000000000000000000, 0.000000000000000000 ) ) ;
#3803=B_SPLINE_CURVE_WITH_KNOTS ( 'NONE', 3,
 ( #12854, #9394, #7034, #14194, #1012, #3393 ),
 .UNSPECIFIED., .F., .F.,
 ( 4, 2, 4 ),
 ( 2.380731629935478318E-07, 0.002336973833157605842, 0.004673709593152217297 ),
 .UNSPECIFIED. ) ;
#3807=LINE ( 'NONE', #7294, #10160 ) ;
#3846=CARTESIAN_POINT ( 'NONE',  ( 0.7145311798163189732, 4.618802153516981868, 8.000000000000007105 ) ) ;
#3848=CARTESIAN_POINT ( 'NONE',  ( 6.399999999999999467, -4.618802153517037823, -7.999999999999979572 ) ) ;
#3879=DIRECTION ( 'NONE',  ( 0.000000000000000000, 0.000000000000000000, 1.000000000000000000 ) ) ;
#3892=ORIENTED_EDGE ( 'NONE', *, *, #5465, .F. ) ;
#3897=ORIENTED_EDGE ( 'NONE', *, *, #4291, .T. ) ;
#3901=ADVANCED_FACE ( 'NONE', ( #12790 ), #14055, .T. ) ;
#3911=ORIENTED_EDGE ( 'NONE', *, *, #2206, .F. ) ;
#3916=CARTESIAN_POINT ( 'NONE',  ( 51.39999999999999858, 0.000000000000000000, 0.000000000000000000 ) ) ;
#3933=DIRECTION ( 'NONE',  ( 0.000000000000000000, -5.551115123125765446E-17, 1.000000000000000000 ) ) ;
#3951=CARTESIAN_POINT ( 'NONE',  ( 0.3167204509598258722, 8.479269695850844002, -1.313474075707198097 ) ) ;
#3958=DIRECTION ( 'NONE',  ( 0.000000000000000000, 0.000000000000000000, -1.000000000000000000 ) ) ;
#3976=ORIENTED_EDGE ( 'NONE', *, *, #2174, .T. ) ;
#4009=ORIENTED_EDGE ( 'NONE', *, *, #3337, .T. ) ;
#4033=DIRECTION ( 'NONE',  ( 0.000000000000000000, 0.000000000000000000, 1.000000000000000000 ) ) ;
#4063=VECTOR ( 'NONE', #15308, 1000.000000000000000 ) ;
#4076=CARTESIAN_POINT ( 'NONE',  ( 6.399999999999999467, 9.797174393178827630E-16, -8.000000000000000000 ) ) ;
#4077=ORIENTED_EDGE ( 'NONE', *, *, #1422, .F. ) ;
#4092=LINE ( 'NONE', #7825, #9192 ) ;
#4094=LINE ( 'NONE', #5207, #5339 ) ;
#4101=ORIENTED_EDGE ( 'NONE', *, *, #14410, .T. ) ;
#4172=TOROIDAL_SURFACE ( 'NONE', #12243, 5.400000000000000355, 0.4000000000000000222 ) ;
#4194=PLANE ( 'NONE',  #14607 ) ;
#4198=EDGE_CURVE ( 'NONE', #1780, #5430, #6011, .T. ) ;
#4246=CARTESIAN_POINT ( 'NONE',  ( 0.3173508448886631639, -8.480771745766420011, -1.310872448937987489 ) ) ;
#4287=VERTEX_POINT ( 'NONE', #4329 ) ;
#4291=EDGE_CURVE ( 'NONE', #4760, #6556, #2069, .T. ) ;
#4292=CARTESIAN_POINT ( 'NONE',  ( 0.000000000000000000, 0.000000000000000000, 0.000000000000000000 ) ) ;
#4306=ORIENTED_EDGE ( 'NONE', *, *, #4974, .F. ) ;
#4308=DIRECTION ( 'NONE',  ( 0.000000000000000000, 0.000000000000000000, -1.000000000000000000 ) ) ;
#4322=CARTESIAN_POINT ( 'NONE',  ( 6.399999999999999467, -4.618802153517037823, -7.999999999999979572 ) ) ;
#4329=CARTESIAN_POINT ( 'NONE',  ( 6.399999999999999467, 0.000000000000000000, -5.400000000000019007 ) ) ;
#4335=AXIS2_PLACEMENT_3D ( 'NONE', #1462, #9776, #14570 ) ;
#4359=B_SPLINE_CURVE_WITH_KNOTS ( 'NONE', 3,
 ( #1074, #1224, #10880, #9691, #6063, #15508, #11821, #11747 ),
 .UNSPECIFIED., .F., .F.,
 ( 4, 2, 2, 4 ),
 ( 0.02285338877108902822, 0.02519297479642219548, 0.02636276780908877737, 0.02753256082175535926 ),
 .UNSPECIFIED. ) ;
#4380=CARTESIAN_POINT ( 'NONE',  ( 0.000000000000000000, 0.000000000000000000, 0.000000000000000000 ) ) ;
#4386=CARTESIAN_POINT ( 'NONE',  ( 0.01688885742776555579, 7.321065037175422674, 3.319543390096038937 ) ) ;
#4400=DIRECTION ( 'NONE',  ( -1.000000000000000000, -0.000000000000000000, -0.000000000000000000 ) ) ;
#4408=ORIENTED_EDGE ( 'NONE', *, *, #5952, .F. ) ;
#4410=DIRECTION ( 'NONE',  ( 0.000000000000000000, 0.000000000000000000, -1.000000000000000000 ) ) ;
#4439=ORIENTED_EDGE ( 'NONE', *, *, #4687, .F. ) ;
#4453=( NAMED_UNIT ( * ) SI_UNIT ( $, .STERADIAN. ) SOLID_ANGLE_UNIT ( ) );
#4462=CARTESIAN_POINT ( 'NONE',  ( 0.000000000000000000, 0.000000000000000000, 0.000000000000000000 ) ) ;
#4568=CARTESIAN_POINT ( 'NONE',  ( 0.000000000000000000, 0.000000000000000000, 0.000000000000000000 ) ) ;
#4592=CARTESIAN_POINT ( 'NONE',  ( 5.799999999999999822, 4.618802153516981868, -7.999999999999979572 ) ) ;
#4611=CARTESIAN_POINT ( 'NONE',  ( 0.7145311798163189732, 4.618802153516981868, 8.000000000000007105 ) ) ;
#4616=CARTESIAN_POINT ( 'NONE',  ( 0.1306530452037929224, 5.952467836904128617, -5.690023276062381008 ) ) ;
#4623=PRODUCT_DEFINITION_SHAPE ( 'NONE', 'NONE',  #14513 ) ;
#4629=ADVANCED_FACE ( 'NONE', ( #14735 ), #5749, .T. ) ;
#4636=DIRECTION ( 'NONE',  ( 0.000000000000000000, 1.000000000000000000, -1.224646799147353207E-16 ) ) ;
#4637=PLANE ( 'NONE',  #13286 ) ;
#4640=DIRECTION ( 'NONE',  ( 0.000000000000000000, 0.000000000000000000, -1.000000000000000000 ) ) ;
#4656=ORIENTED_EDGE ( 'NONE', *, *, #6397, .F. ) ;
#4672=DIRECTION ( 'NONE',  ( 0.000000000000000000, 0.000000000000000000, 1.000000000000000000 ) ) ;
#4687=EDGE_CURVE ( 'NONE', #1780, #11026, #7575, .T. ) ;
#4716=EDGE_CURVE ( 'NONE', #50, #14309, #3729, .T. ) ;
#4726=FACE_OUTER_BOUND ( 'NONE', #11382, .T. ) ;
#4760=VERTEX_POINT ( 'NONE', #5197 ) ;
#4784=ORIENTED_EDGE ( 'NONE', *, *, #12679, .T. ) ;
#4788=CARTESIAN_POINT ( 'NONE',  ( 0.000000000000000000, 0.000000000000000000, 8.000000000000007105 ) ) ;
#4795=CIRCLE ( 'NONE', #12590, 8.000000000000028422 ) ;
#4798=CARTESIAN_POINT ( 'NONE',  ( 0.4973051450695574749, -3.866309095700866116, -7.999999999999979572 ) ) ;
#4807=ORIENTED_EDGE ( 'NONE', *, *, #4291, .F. ) ;
#4837=AXIS2_PLACEMENT_3D ( 'NONE', #11526, #2931, #6649 ) ;
#4866=EDGE_LOOP ( 'NONE', ( #9285, #3976, #9808 ) ) ;
#4918=VERTEX_POINT ( 'NONE', #11513 ) ;
#4974=EDGE_CURVE ( 'NONE', #14204, #908, #1452, .T. ) ;
#5030=DIRECTION ( 'NONE',  ( -1.000000000000000000, 0.000000000000000000, 0.000000000000000000 ) ) ;
#5032=CARTESIAN_POINT ( 'NONE',  ( 0.000000000000000000, 0.000000000000000000, 0.000000000000000000 ) ) ;
#5040=DIRECTION ( 'NONE',  ( -1.000000000000000000, 0.000000000000000000, 0.000000000000000000 ) ) ;
#5048=VERTEX_POINT ( 'NONE', #13569 ) ;
#5074=CARTESIAN_POINT ( 'NONE',  ( 6.800000000000000711, 0.000000000000000000, 0.000000000000000000 ) ) ;
#5195=ORIENTED_EDGE ( 'NONE', *, *, #624, .F. ) ;
#5197=CARTESIAN_POINT ( 'NONE',  ( 0.000000000000000000, -6.928203230275514990, -4.000000000000003553 ) ) ;
#5206=UNCERTAINTY_MEASURE_WITH_UNIT (LENGTH_MEASURE( 1.000000000000000082E-05 ), #5727, 'distance_accuracy_value', 'NONE');
#5207=CARTESIAN_POINT ( 'NONE',  ( 5.799999999999999822, -4.618802153517037823, -7.999999999999979572 ) ) ;
#5217=CARTESIAN_POINT ( 'NONE',  ( 0.7145311798163258565, 9.237604307034018802, 0.000000000000000000 ) ) ;
#5226=FACE_OUTER_BOUND ( 'NONE', #9470, .T. ) ;
#5291=ORIENTED_EDGE ( 'NONE', *, *, #10684, .T. ) ;
#5306=ORIENTED_EDGE ( 'NONE', *, *, #10203, .F. ) ;
#5318=AXIS2_PLACEMENT_3D ( 'NONE', #4462, #12987, #4308 ) ;
#5319=LINE ( 'NONE', #9038, #11336 ) ;
#5320=ORIENTED_EDGE ( 'NONE', *, *, #2331, .T. ) ;
#5339=VECTOR ( 'NONE', #12384, 1000.000000000000000 ) ;
#5358=MECHANICAL_DESIGN_GEOMETRIC_PRESENTATION_REPRESENTATION('',(#15177),#12660);
#5382=ORIENTED_EDGE ( 'NONE', *, *, #791, .T. ) ;
#5397=AXIS2_PLACEMENT_3D ( 'NONE', #4322, #13962, #3145 ) ;
#5422=ORIENTED_EDGE ( 'NONE', *, *, #10755, .F. ) ;
#5430=VERTEX_POINT ( 'NONE', #10423 ) ;
#5465=EDGE_CURVE ( 'NONE', #8637, #1780, #13240, .T. ) ;
#5479=CARTESIAN_POINT ( 'NONE',  ( 6.399999999999999467, 4.618802153516981868, 8.000000000000007105 ) ) ;
#5484=DIRECTION ( 'NONE',  ( 0.000000000000000000, -0.5000000000000012212, 0.8660254037844380415 ) ) ;
#5505=DIRECTION ( 'NONE',  ( 0.000000000000000000, 0.000000000000000000, -1.000000000000000000 ) ) ;
#5509=ORIENTED_EDGE ( 'NONE', *, *, #6344, .F. ) ;
#5513=CARTESIAN_POINT ( 'NONE',  ( 6.399999999999999467, 4.618802153516981868, -7.999999999999979572 ) ) ;
#5533=DIRECTION ( 'NONE',  ( 0.000000000000000000, -0.5000000000000019984, -0.8660254037844375974 ) ) ;
#5598=CARTESIAN_POINT ( 'NONE',  ( 6.399999999999999467, 0.000000000000000000, 0.000000000000000000 ) ) ;
#5619=ORIENTED_EDGE ( 'NONE', *, *, #3073, .T. ) ;
#5636=ADVANCED_FACE ( 'NONE', ( #14738 ), #12523, .F. ) ;
#5664=VERTEX_POINT ( 'NONE', #14023 ) ;
#5681=DIRECTION ( 'NONE',  ( 1.000000000000000000, 0.000000000000000000, 0.000000000000000000 ) ) ;
#5683=CARTESIAN_POINT ( 'NONE',  ( 3.011202127489036917E-15, -7.124194613927635977, -3.660532965668818584 ) ) ;
#5703=AXIS2_PLACEMENT_3D ( 'NONE', #3048, #1849, #2087 ) ;
#5727=( LENGTH_UNIT ( ) NAMED_UNIT ( * ) SI_UNIT ( .MILLI., .METRE. ) );
#5749=CONICAL_SURFACE ( 'NONE', #15062, 4.172000000000013920, 0.7853981633974430610 ) ;
#5766=CARTESIAN_POINT ( 'NONE',  ( 0.000000000000000000, 0.000000000000000000, 8.000000000000007105 ) ) ;
#5780=CIRCLE ( 'NONE', #6806, 8.000000000000028422 ) ;
#5799=CARTESIAN_POINT ( 'NONE',  ( -4.651904946320617462E-15, 6.534749472788140778, 4.681481898397007235 ) ) ;
#5837=CARTESIAN_POINT ( 'NONE',  ( 0.000000000000000000, 0.000000000000000000, 8.000000000000028422 ) ) ;
#5842=AXIS2_PLACEMENT_3D ( 'NONE', #3668, #2408, #12114 ) ;
#5846=B_SPLINE_CURVE_WITH_KNOTS ( 'NONE', 3,
 ( #5217, #2935, #3951, #6494, #1733, #14680 ),
 .UNSPECIFIED., .F., .F.,
 ( 4, 2, 4 ),
 ( 2.380731629557702153E-07, 0.002336973833157555101, 0.004673709593152154847 ),
 .UNSPECIFIED. ) ;
#5864=DIRECTION ( 'NONE',  ( 0.000000000000000000, 0.5000000000000013323, 0.8660254037844380415 ) ) ;
#5879=AXIS2_PLACEMENT_3D ( 'NONE', #7842, #11457, #14122 ) ;
#5886=EDGE_LOOP ( 'NONE', ( #14459, #12036 ) ) ;
#5888=CIRCLE ( 'NONE', #9419, 8.000000000000028422 ) ;
#5952=EDGE_CURVE ( 'NONE', #8751, #10460, #14594, .T. ) ;
#5995=CARTESIAN_POINT ( 'NONE',  ( 0.000000000000000000, 6.928203230275487456, 4.000000000000003553 ) ) ;
#6005=EDGE_CURVE ( 'NONE', #5048, #4760, #7662, .T. ) ;
#6006=CARTESIAN_POINT ( 'NONE',  ( 0.06730325657896824021, -1.557442666625485250, 8.000000000000008882 ) ) ;
#6011=LINE ( 'NONE', #3562, #6289 ) ;
#6063=CARTESIAN_POINT ( 'NONE',  ( 0.08285530295197468531, 1.570896314769965940, -7.999999999999981348 ) ) ;
#6081=DIRECTION ( 'NONE',  ( 0.000000000000000000, 0.000000000000000000, 1.000000000000000000 ) ) ;
#6098=AXIS2_PLACEMENT_3D ( 'NONE', #3228, #15217, #4410 ) ;
#6104=AXIS2_PLACEMENT_3D ( 'NONE', #4380, #2010, #6695 ) ;
#6109=DIRECTION ( 'NONE',  ( 1.000000000000000000, 0.000000000000000000, 0.000000000000000000 ) ) ;
#6170=CONICAL_SURFACE ( 'NONE', #1624, 8.000000000000028422, 1.047197551196600296 ) ;
#6209=DIRECTION ( 'NONE',  ( 0.000000000000000000, -0.5000000000000012212, -0.8660254037844379305 ) ) ;
#6232=PRESENTATION_STYLE_ASSIGNMENT (( #14271 ) ) ;
#6289=VECTOR ( 'NONE', #14519, 999.9999999999998863 ) ;
#6294=EDGE_CURVE ( 'NONE', #4760, #2448, #5780, .T. ) ;
#6324=AXIS2_PLACEMENT_3D ( 'NONE', #3916, #5030, #2425 ) ;
#6344=EDGE_CURVE ( 'NONE', #8637, #14616, #2502, .T. ) ;
#6361=VECTOR ( 'NONE', #10030, 1000.000000000000000 ) ;
#6375=CIRCLE ( 'NONE', #4335, 8.000000000000028422 ) ;
#6383=COLOUR_RGB ( '', 0.09019608, 0.27058824, 0.51372549) ;
#6389=ORIENTED_EDGE ( 'NONE', *, *, #7544, .T. ) ;
#6390=EDGE_CURVE ( 'NONE', #3554, #14309, #13123, .T. ) ;
#6397=EDGE_CURVE ( 'NONE', #2142, #326, #3014, .T. ) ;
#6428=ORIENTED_EDGE ( 'NONE', *, *, #10975, .T. ) ;
#6465=CARTESIAN_POINT ( 'NONE',  ( 5.799999999999999822, 4.618802153516981868, 8.000000000000007105 ) ) ;
#6466=ORIENTED_EDGE ( 'NONE', *, *, #2174, .F. ) ;
#6472=DIRECTION ( 'NONE',  ( 0.000000000000000000, 0.000000000000000000, 1.000000000000000000 ) ) ;
#6494=CARTESIAN_POINT ( 'NONE',  ( 0.06809871960541388769, 7.710219529346588274, -2.645508037661862932 ) ) ;
#6513=AXIS2_PLACEMENT_3D ( 'NONE', #8948, #11229, #4033 ) ;
#6543=EDGE_CURVE ( 'NONE', #4287, #6660, #9329, .T. ) ;
#6551=DIRECTION ( 'NONE',  ( -1.000000000000000000, 0.000000000000000000, 0.000000000000000000 ) ) ;
#6556=VERTEX_POINT ( 'NONE', #6596 ) ;
#6566=AXIS2_PLACEMENT_3D ( 'NONE', #8960, #12562, #1757 ) ;
#6570=FACE_OUTER_BOUND ( 'NONE', #10273, .T. ) ;
#6586=FACE_OUTER_BOUND ( 'NONE', #6857, .T. ) ;
#6596=CARTESIAN_POINT ( 'NONE',  ( 0.7145311798163258565, -9.237604307034018802, 2.775557561562891351E-14 ) ) ;
#6626=ADVANCED_FACE ( 'NONE', ( #4726 ), #4194, .F. ) ;
#6649=DIRECTION ( 'NONE',  ( 0.000000000000000000, 0.000000000000000000, -1.000000000000000000 ) ) ;
#6660=VERTEX_POINT ( 'NONE', #11635 ) ;
#6665=ADVANCED_FACE ( 'NONE', ( #13166 ), #10448, .F. ) ;
#6676=CARTESIAN_POINT ( 'NONE',  ( 50.57199999999998852, 0.000000000000000000, 5.000000000000017764 ) ) ;
#6680=ADVANCED_FACE ( 'NONE', ( #8095 ), #12880, .T. ) ;
#6695=DIRECTION ( 'NONE',  ( 0.000000000000000000, 0.000000000000000000, -1.000000000000000000 ) ) ;
#6715=PLANE ( 'NONE',  #5397 ) ;
#6730=ORIENTED_EDGE ( 'NONE', *, *, #338, .F. ) ;
#6743=ORIENTED_EDGE ( 'NONE', *, *, #44, .T. ) ;
#6758=ORIENTED_EDGE ( 'NONE', *, *, #3337, .F. ) ;
#6769=DIRECTION ( 'NONE',  ( 0.000000000000000000, 0.000000000000000000, 1.000000000000000000 ) ) ;
#6796=EDGE_LOOP ( 'NONE', ( #9087, #8271, #8718, #11957 ) ) ;
#6806=AXIS2_PLACEMENT_3D ( 'NONE', #4292, #10384, #10309 ) ;
#6853=CARTESIAN_POINT ( 'NONE',  ( 0.1306530452038093260, 7.903938623646864059, 2.309976723937613663 ) ) ;
#6857=EDGE_LOOP ( 'NONE', ( #11428, #9594, #13314 ) ) ;
#6879=ORIENTED_EDGE ( 'NONE', *, *, #3740, .F. ) ;
#6884=ORIENTED_EDGE ( 'NONE', *, *, #12857, .F. ) ;
#6891=DIRECTION ( 'NONE',  ( 1.000000000000000000, 0.000000000000000000, 0.000000000000000000 ) ) ;
#6960=ADVANCED_FACE ( 'NONE', ( #14721 ), #8593, .T. ) ;
#6962=EDGE_CURVE ( 'NONE', #2861, #5048, #9770, .T. ) ;
#7010=CARTESIAN_POINT ( 'NONE',  ( 5.799999999999999822, 7.999999999999979572, 0.000000000000000000 ) ) ;
#7022=DIRECTION ( 'NONE',  ( 0.000000000000000000, 0.000000000000000000, -1.000000000000000000 ) ) ;
#7034=CARTESIAN_POINT ( 'NONE',  ( 0.3167204509598386397, -8.479269695850858213, 1.313474075707245392 ) ) ;
#7048=ORIENTED_EDGE ( 'NONE', *, *, #1028, .F. ) ;
#7055=CARTESIAN_POINT ( 'NONE',  ( 5.799999999999999822, 9.237604307034018802, 0.000000000000000000 ) ) ;
#7093=DIRECTION ( 'NONE',  ( 0.000000000000000000, 0.000000000000000000, -1.000000000000000000 ) ) ;
#7100=CARTESIAN_POINT ( 'NONE',  ( -1.014660767515926061E-14, -0.7818963812181285444, -7.999999999999981348 ) ) ;
#7113=( NAMED_UNIT ( * ) PLANE_ANGLE_UNIT ( ) SI_UNIT ( $, .RADIAN. ) );
#7124=ORIENTED_EDGE ( 'NONE', *, *, #7965, .F. ) ;
#7141=DIRECTION ( 'NONE',  ( -1.000000000000000000, 0.000000000000000000, 0.000000000000000000 ) ) ;
#7176=FACE_OUTER_BOUND ( 'NONE', #4866, .T. ) ;
#7182=AXIS2_PLACEMENT_3D ( 'NONE', #5032, #183, #3767 ) ;
#7187=CARTESIAN_POINT ( 'NONE',  ( 0.000000000000000000, 9.237604307034018802, 0.000000000000000000 ) ) ;
#7192=ORIENTED_EDGE ( 'NONE', *, *, #318, .T. ) ;
#7227=DIRECTION ( 'NONE',  ( -0.7071067811865500152, 0.000000000000000000, 0.7071067811865451302 ) ) ;
#7247=ORIENTED_EDGE ( 'NONE', *, *, #8923, .F. ) ;
#7294=CARTESIAN_POINT ( 'NONE',  ( 5.799999999999999822, -4.618802153517037823, -7.999999999999979572 ) ) ;
#7317=EDGE_LOOP ( 'NONE', ( #6428, #2721, #6389 ) ) ;
#7338=CARTESIAN_POINT ( 'NONE',  ( 0.000000000000000000, -2.775557561562891351E-14, -8.000000000000007105 ) ) ;
#7408=DIRECTION ( 'NONE',  ( 1.000000000000000000, 0.000000000000000000, 0.000000000000000000 ) ) ;
#7410=CARTESIAN_POINT ( 'NONE',  ( 0.3194001229790410235, 3.115132258388565667, 8.000000000000007105 ) ) ;
#7425=SURFACE_STYLE_FILL_AREA ( #13239 ) ;
#7426=DIRECTION ( 'NONE',  ( 0.000000000000000000, 0.5000000000000013323, 0.8660254037844380415 ) ) ;
#7472=EDGE_LOOP ( 'NONE', ( #11933, #14057, #4077, #6758, #12596, #8404 ) ) ;
#7497=CARTESIAN_POINT ( 'NONE',  ( 5.799999999999999822, 4.618802153516981868, -7.999999999999979572 ) ) ;
#7531=EDGE_LOOP ( 'NONE', ( #13358, #8710, #15582, #10417 ) ) ;
#7540=AXIS2_PLACEMENT_3D ( 'NONE', #12714, #7930, #13020 ) ;
#7544=EDGE_CURVE ( 'NONE', #1809, #5430, #4795, .T. ) ;
#7555=ORIENTED_EDGE ( 'NONE', *, *, #8743, .F. ) ;
#7559=CARTESIAN_POINT ( 'NONE',  ( 0.4964154566687650205, -4.996589667937459289, -7.345652830558652369 ) ) ;
#7575=LINE ( 'NONE', #8753, #950 ) ;
#7643=CARTESIAN_POINT ( 'NONE',  ( 5.799999999999999822, 7.999999999999979572, 0.000000000000000000 ) ) ;
#7658=DIRECTION ( 'NONE',  ( -1.000000000000000000, 0.000000000000000000, 0.000000000000000000 ) ) ;
#7662=B_SPLINE_CURVE_WITH_KNOTS ( 'NONE', 3,
 ( #2734, #7559, #1621, #8814, #10006, #7877 ),
 .UNSPECIFIED., .F., .F.,
 ( 4, 2, 4 ),
 ( 2.380731630556046949E-07, 0.002336973833157585459, 0.004673709593152115815 ),
 .UNSPECIFIED. ) ;
#7677=ORIENTED_EDGE ( 'NONE', *, *, #338, .T. ) ;
#7704=DIRECTION ( 'NONE',  ( -1.000000000000000000, 0.000000000000000000, 0.000000000000000000 ) ) ;
#7725=DIRECTION ( 'NONE',  ( 0.000000000000000000, 0.000000000000000000, 1.000000000000000000 ) ) ;
#7746=FACE_OUTER_BOUND ( 'NONE', #15506, .T. ) ;
#7762=ORIENTED_EDGE ( 'NONE', *, *, #10129, .T. ) ;
#7793=EDGE_CURVE ( 'NONE', #14616, #14639, #10293, .T. ) ;
#7825=CARTESIAN_POINT ( 'NONE',  ( 51.39999999999999858, 5.109226446042775356E-16, -4.172000000000013920 ) ) ;
#7842=CARTESIAN_POINT ( 'NONE',  ( 5.799999999999999822, 7.999999999999979572, 0.000000000000000000 ) ) ;
#7850=DIRECTION ( 'NONE',  ( 0.000000000000000000, 0.000000000000000000, -1.000000000000000000 ) ) ;
#7877=CARTESIAN_POINT ( 'NONE',  ( 0.000000000000000000, -6.928203230275514990, -4.000000000000003553 ) ) ;
#7900=EDGE_CURVE ( 'NONE', #14639, #8637, #1039, .T. ) ;
#7927=DIRECTION ( 'NONE',  ( 1.000000000000000000, 0.000000000000000000, 0.000000000000000000 ) ) ;
#7930=DIRECTION ( 'NONE',  ( -1.000000000000000000, 0.000000000000000000, 0.000000000000000000 ) ) ;
#7936=CARTESIAN_POINT ( 'NONE',  ( 0.000000000000000000, 0.000000000000000000, 0.000000000000000000 ) ) ;
#7963=DIRECTION ( 'NONE',  ( 1.000000000000000000, 0.000000000000000000, 0.000000000000000000 ) ) ;
#7965=EDGE_CURVE ( 'NONE', #5664, #2142, #3807, .T. ) ;
#8094=VECTOR ( 'NONE', #7227, 1000.000000000000114 ) ;
#8095=FACE_OUTER_BOUND ( 'NONE', #11461, .T. ) ;
#8114=CYLINDRICAL_SURFACE ( 'NONE', #5703, 8.000000000000028422 ) ;
#8117=CONICAL_SURFACE ( 'NONE', #1276, 8.000000000000028422, 1.047197551196600296 ) ;
#8147=DIRECTION ( 'NONE',  ( 0.000000000000000000, 0.000000000000000000, 1.000000000000000000 ) ) ;
#8150=CARTESIAN_POINT ( 'NONE',  ( 0.7145311798163258565, -9.237604307034018802, 2.775557561562891351E-14 ) ) ;
#8158=EDGE_LOOP ( 'NONE', ( #7762, #2625 ) ) ;
#8159=ORIENTED_EDGE ( 'NONE', *, *, #1505, .F. ) ;
#8163=EDGE_LOOP ( 'NONE', ( #6743, #14267, #3897 ) ) ;
#8165=CARTESIAN_POINT ( 'NONE',  ( 0.000000000000000000, 9.797174393178861156E-16, -8.000000000000028422 ) ) ;
#8207=CARTESIAN_POINT ( 'NONE',  ( 5.799999999999999822, 7.999999999999979572, 0.000000000000000000 ) ) ;
#8251=ADVANCED_FACE ( 'NONE', ( #2046 ), #11693, .T. ) ;
#8267=( NAMED_UNIT ( * ) PLANE_ANGLE_UNIT ( ) SI_UNIT ( $, .RADIAN. ) );
#8271=ORIENTED_EDGE ( 'NONE', *, *, #4974, .T. ) ;
#8319=DIRECTION ( 'NONE',  ( 0.000000000000000000, 0.000000000000000000, -1.000000000000000000 ) ) ;
#8333=AXIS2_PLACEMENT_3D ( 'NONE', #7010, #14483, #7093 ) ;
#8362=AXIS2_PLACEMENT_3D ( 'NONE', #14016, #7963, #12914 ) ;
#8368=DIRECTION ( 'NONE',  ( 0.000000000000000000, 1.224646799147353207E-16, 1.000000000000000000 ) ) ;
#8388=APPLICATION_CONTEXT ( 'automotive_design' ) ;
#8392=VERTEX_POINT ( 'NONE', #2022 ) ;
#8404=ORIENTED_EDGE ( 'NONE', *, *, #10975, .F. ) ;
#8445=CIRCLE ( 'NONE', #7182, 8.000000000000028422 ) ;
#8453=VERTEX_POINT ( 'NONE', #10327 ) ;
#8479=CIRCLE ( 'NONE', #1146, 5.000000000000017764 ) ;
#8530=DIRECTION ( 'NONE',  ( -1.000000000000000000, 0.000000000000000000, 0.000000000000000000 ) ) ;
#8549=CARTESIAN_POINT ( 'NONE',  ( 5.799999999999999822, 4.618802153516981868, -7.999999999999979572 ) ) ;
#8593=CONICAL_SURFACE ( 'NONE', #6324, 4.172000000000013920, 0.7853981633974430610 ) ;
#8594=DIRECTION ( 'NONE',  ( 0.000000000000000000, 0.000000000000000000, -1.000000000000000000 ) ) ;
#8620=VECTOR ( 'NONE', #9546, 1000.000000000000000 ) ;
#8637=VERTEX_POINT ( 'NONE', #10956 ) ;
#8673=ADVANCED_FACE ( 'NONE', ( #7176 ), #11350, .T. ) ;
#8675=CARTESIAN_POINT ( 'NONE',  ( 6.800000000000000711, 0.000000000000000000, 5.000000000000000000 ) ) ;
#8710=ORIENTED_EDGE ( 'NONE', *, *, #11002, .T. ) ;
#8718=ORIENTED_EDGE ( 'NONE', *, *, #8923, .T. ) ;
#8743=EDGE_CURVE ( 'NONE', #10266, #8392, #15545, .T. ) ;
#8744=DIRECTION ( 'NONE',  ( -1.000000000000000000, 0.000000000000000000, 0.000000000000000000 ) ) ;
#8751=VERTEX_POINT ( 'NONE', #3104 ) ;
#8753=CARTESIAN_POINT ( 'NONE',  ( 6.399999999999999467, 9.237604307034018802, 0.000000000000000000 ) ) ;
#8755=DIRECTION ( 'NONE',  ( 1.000000000000000000, 0.000000000000000000, 0.000000000000000000 ) ) ;
#8787=CARTESIAN_POINT ( 'NONE',  ( 5.799999999999999822, 7.999999999999979572, 0.000000000000000000 ) ) ;
#8797=DIRECTION ( 'NONE',  ( 0.000000000000000000, 0.000000000000000000, 1.000000000000000000 ) ) ;
#8814=CARTESIAN_POINT ( 'NONE',  ( 0.06809871960543052716, -6.146186931204450588, -5.354491962338080668 ) ) ;
#8825=LINE ( 'NONE', #6465, #9082 ) ;
#8859=VECTOR ( 'NONE', #5533, 999.9999999999998863 ) ;
#8884=CONICAL_SURFACE ( 'NONE', #6104, 8.000000000000028422, 1.047197551196600296 ) ;
#8901=DIRECTION ( 'NONE',  ( -1.000000000000000000, 0.000000000000000000, 0.000000000000000000 ) ) ;
#8923=EDGE_CURVE ( 'NONE', #908, #3554, #14457, .T. ) ;
#8926=DIRECTION ( 'NONE',  ( 0.000000000000000000, 0.000000000000000000, -1.000000000000000000 ) ) ;
#8934=PLANE ( 'NONE',  #6098 ) ;
#8948=CARTESIAN_POINT ( 'NONE',  ( 51.39999999999999858, 0.000000000000000000, 0.000000000000000000 ) ) ;
#8960=CARTESIAN_POINT ( 'NONE',  ( 6.399999999999999467, 0.000000000000000000, 0.000000000000000000 ) ) ;
#8977=TOROIDAL_SURFACE ( 'NONE', #373, 5.400000000000000355, 0.4000000000000000222 ) ;
#9008=CARTESIAN_POINT ( 'NONE',  ( 0.4969600502617610993, -8.860760056385762695, -0.6527133886630168691 ) ) ;
#9013=DIRECTION ( 'NONE',  ( -1.000000000000000000, 0.000000000000000000, 0.000000000000000000 ) ) ;
#9038=CARTESIAN_POINT ( 'NONE',  ( 5.799999999999999822, 9.237604307034018802, 0.000000000000000000 ) ) ;
#9041=AXIS2_PLACEMENT_3D ( 'NONE', #3203, #743, #6769 ) ;
#9074=AXIS2_PLACEMENT_3D ( 'NONE', #9827, #3737, #13361 ) ;
#9082=VECTOR ( 'NONE', #11270, 1000.000000000000000 ) ;
#9087=ORIENTED_EDGE ( 'NONE', *, *, #13676, .F. ) ;
#9115=DIRECTION ( 'NONE',  ( -1.000000000000000000, 0.000000000000000000, 0.000000000000000000 ) ) ;
#9128=UNCERTAINTY_MEASURE_WITH_UNIT (LENGTH_MEASURE( 1.000000000000000082E-05 ), #13081, 'distance_accuracy_value', 'NONE');
#9181=ORIENTED_EDGE ( 'NONE', *, *, #1505, .T. ) ;
#9192=VECTOR ( 'NONE', #9232, 1000.000000000000114 ) ;
#9193=DIRECTION ( 'NONE',  ( 0.000000000000000000, 0.8660254037844375974, -0.5000000000000019984 ) ) ;
#9217=CARTESIAN_POINT ( 'NONE',  ( 0.08224679563971239171, 7.710515798486361483, 2.644994884459111795 ) ) ;
#9232=DIRECTION ( 'NONE',  ( -0.7071067811865500152, 8.659560562354904508E-17, -0.7071067811865451302 ) ) ;
#9244=ORIENTED_EDGE ( 'NONE', *, *, #2331, .F. ) ;
#9246=LINE ( 'NONE', #13973, #8859 ) ;
#9253=EDGE_LOOP ( 'NONE', ( #6730, #4306 ) ) ;
#9282=FACE_OUTER_BOUND ( 'NONE', #13747, .T. ) ;
#9285=ORIENTED_EDGE ( 'NONE', *, *, #1422, .T. ) ;
#9326=ORIENTED_EDGE ( 'NONE', *, *, #14410, .F. ) ;
#9328=ORIENTED_EDGE ( 'NONE', *, *, #10129, .F. ) ;
#9329=CIRCLE ( 'NONE', #6566, 5.400000000000019007 ) ;
#9335=LINE ( 'NONE', #8165, #11743 ) ;
#9394=CARTESIAN_POINT ( 'NONE',  ( 0.4964154566687934422, -8.859816792613649739, 0.6543471694412702488 ) ) ;
#9398=ADVANCED_FACE ( 'NONE', ( #10549 ), #3368, .T. ) ;
#9417=ADVANCED_FACE ( 'NONE', ( #11580, #829 ), #905, .T. ) ;
#9418=DIRECTION ( 'NONE',  ( 0.000000000000000000, 1.000000000000000000, 0.000000000000000000 ) ) ;
#9419=AXIS2_PLACEMENT_3D ( 'NONE', #9462, #13147, #995 ) ;
#9434=EDGE_CURVE ( 'NONE', #379, #207, #775, .T. ) ;
#9451=CARTESIAN_POINT ( 'NONE',  ( 0.000000000000000000, 6.928203230275487456, 4.000000000000003553 ) ) ;
#9462=CARTESIAN_POINT ( 'NONE',  ( 0.000000000000000000, 0.000000000000000000, 0.000000000000000000 ) ) ;
#9463=CARTESIAN_POINT ( 'NONE',  ( 0.3157512944565224466, -3.097794232830199057, -7.999999999999979572 ) ) ;
#9470=EDGE_LOOP ( 'NONE', ( #14991, #13419, #1748, #14673 ) ) ;
#9497=DIRECTION ( 'NONE',  ( 0.000000000000000000, 0.4999999999999996669, -0.8660254037844388186 ) ) ;
#9520=CARTESIAN_POINT ( 'NONE',  ( 6.399999999999999467, 4.618802153516981868, 8.000000000000007105 ) ) ;
#9546=DIRECTION ( 'NONE',  ( -1.000000000000000000, 0.000000000000000000, 0.000000000000000000 ) ) ;
#9594=ORIENTED_EDGE ( 'NONE', *, *, #4198, .T. ) ;
#9604=DIRECTION ( 'NONE',  ( -1.000000000000000000, 0.000000000000000000, 0.000000000000000000 ) ) ;
#9679=DIRECTION ( 'NONE',  ( 0.000000000000000000, 0.000000000000000000, 1.000000000000000000 ) ) ;
#9689=EDGE_LOOP ( 'NONE', ( #14928, #9181, #2646 ) ) ;
#9691=CARTESIAN_POINT ( 'NONE',  ( 0.1317522424471971043, 1.959574484719836196, -7.999999999999977796 ) ) ;
#9770=LINE ( 'NONE', #3848, #14113 ) ;
#9776=DIRECTION ( 'NONE',  ( 1.000000000000000000, 0.000000000000000000, 0.000000000000000000 ) ) ;
#9792=CIRCLE ( 'NONE', #9041, 5.000000000000017764 ) ;
#9808=ORIENTED_EDGE ( 'NONE', *, *, #9434, .T. ) ;
#9818=DIRECTION ( 'NONE',  ( 1.000000000000000000, 0.000000000000000000, 0.000000000000000000 ) ) ;
#9827=CARTESIAN_POINT ( 'NONE',  ( 5.799999999999999822, 0.000000000000000000, 0.000000000000000000 ) ) ;
#9839=DIRECTION ( 'NONE',  ( -1.000000000000000000, 0.000000000000000000, 0.000000000000000000 ) ) ;
#9852=ADVANCED_FACE ( 'NONE', ( #11860 ), #8117, .T. ) ;
#9854=CARTESIAN_POINT ( 'NONE',  ( 0.1317522424472134801, 1.959574484719845300, 8.000000000000007105 ) ) ;
#9878=CLOSED_SHELL ( 'NONE', ( #12502, #3237, #4629, #11536, #9417, #3901, #6960, #13895, #13465, #15349, #8251, #1464, #9398, #10089, #6680, #13784, #8673, #9852, #11435, #10582, #415, #13692, #5636, #13733, #6626, #6665, #12684, #14812, #12757 ) ) ;
#9890=CONICAL_SURFACE ( 'NONE', #5842, 8.000000000000028422, 1.047197551196600296 ) ;
#9895=ORIENTED_EDGE ( 'NONE', *, *, #10969, .F. ) ;
#9924=EDGE_CURVE ( 'NONE', #14943, #1809, #1109, .T. ) ;
#9930=LINE ( 'NONE', #14720, #11768 ) ;
#10006=CARTESIAN_POINT ( 'NONE',  ( 3.233971792616918695E-15, -6.534749472788175417, -4.681481898396977925 ) ) ;
#10014=CARTESIAN_POINT ( 'NONE',  ( 0.000000000000000000, 0.000000000000000000, 0.000000000000000000 ) ) ;
#10027=EDGE_LOOP ( 'NONE', ( #14135, #14406, #12655 ) ) ;
#10030=DIRECTION ( 'NONE',  ( 0.000000000000000000, 1.000000000000000000, 0.000000000000000000 ) ) ;
#10064=AXIS2_PLACEMENT_3D ( 'NONE', #1532, #10950, #6209 ) ;
#10089=ADVANCED_FACE ( 'NONE', ( #6570 ), #8934, .T. ) ;
#10129=EDGE_CURVE ( 'NONE', #8453, #1214, #784, .T. ) ;
#10160=VECTOR ( 'NONE', #9497, 1000.000000000000000 ) ;
#10192=EDGE_LOOP ( 'NONE', ( #105, #4009, #11705 ) ) ;
#10195=CARTESIAN_POINT ( 'NONE',  ( 5.799999999999999822, 0.000000000000000000, 0.000000000000000000 ) ) ;
#10198=AXIS2_PLACEMENT_3D ( 'NONE', #13072, #2351, #3538 ) ;
#10199=B_SPLINE_CURVE_WITH_KNOTS ( 'NONE', 3,
 ( #7338, #7100, #13148, #9463, #4798, #14262 ),
 .UNSPECIFIED., .F., .F.,
 ( 4, 2, 4 ),
 ( 0.02753256082175535926, 0.02987018134127081975, 0.03220780186078627677 ),
 .UNSPECIFIED. ) ;
#10203=EDGE_CURVE ( 'NONE', #8453, #1809, #3391, .T. ) ;
#10219=CARTESIAN_POINT ( 'NONE',  ( 5.799999999999999822, 0.000000000000000000, 0.000000000000000000 ) ) ;
#10226=ORIENTED_EDGE ( 'NONE', *, *, #6962, .T. ) ;
#10264=CARTESIAN_POINT ( 'NONE',  ( 0.000000000000000000, -6.928203230275514990, -4.000000000000003553 ) ) ;
#10266=VERTEX_POINT ( 'NONE', #930 ) ;
#10273=EDGE_LOOP ( 'NONE', ( #3103, #5382, #2874 ) ) ;
#10286=CARTESIAN_POINT ( 'NONE',  ( 0.01688885742777249468, -6.535341423375579772, 4.680456609904006804 ) ) ;
#10293=LINE ( 'NONE', #4592, #14856 ) ;
#10309=DIRECTION ( 'NONE',  ( 0.000000000000000000, 0.000000000000000000, -1.000000000000000000 ) ) ;
#10322=DIRECTION ( 'NONE',  ( 1.000000000000000000, 0.000000000000000000, 0.000000000000000000 ) ) ;
#10327=CARTESIAN_POINT ( 'NONE',  ( 6.399999999999999467, 0.000000000000000000, 8.000000000000000000 ) ) ;
#10341=AXIS2_PLACEMENT_3D ( 'NONE', #14937, #2883, #11639 ) ;
#10360=ORIENTED_EDGE ( 'NONE', *, *, #14574, .T. ) ;
#10370=EDGE_CURVE ( 'NONE', #5430, #8637, #11386, .T. ) ;
#10384=DIRECTION ( 'NONE',  ( 1.000000000000000000, 0.000000000000000000, 0.000000000000000000 ) ) ;
#10417=ORIENTED_EDGE ( 'NONE', *, *, #12338, .T. ) ;
#10423=CARTESIAN_POINT ( 'NONE',  ( 5.799999999999999822, 6.928203230275487456, 4.000000000000003553 ) ) ;
#10448=PLANE ( 'NONE',  #13602 ) ;
#10460=VERTEX_POINT ( 'NONE', #282 ) ;
#10488=EDGE_CURVE ( 'NONE', #2142, #2861, #4094, .T. ) ;
#10511=FACE_OUTER_BOUND ( 'NONE', #7472, .T. ) ;
#10522=CARTESIAN_POINT ( 'NONE',  ( 0.7145311798163258565, 9.237604307034018802, 0.000000000000000000 ) ) ;
#10549=FACE_OUTER_BOUND ( 'NONE', #10712, .T. ) ;
#10556=VECTOR ( 'NONE', #9604, 1000.000000000000000 ) ;
#10582=ADVANCED_FACE ( 'NONE', ( #14009 ), #8884, .T. ) ;
#10618=ORIENTED_EDGE ( 'NONE', *, *, #14701, .F. ) ;
#10645=CARTESIAN_POINT ( 'NONE',  ( 6.800000000000000711, 6.613092715395731132E-16, 5.400000000000019007 ) ) ;
#10669=FACE_OUTER_BOUND ( 'NONE', #1031, .T. ) ;
#10684=EDGE_CURVE ( 'NONE', #12934, #50, #11338, .T. ) ;
#10703=CARTESIAN_POINT ( 'NONE',  ( -1.931933921921289571E-14, 6.732211846623371798, -4.339467034331174311 ) ) ;
#10712=EDGE_LOOP ( 'NONE', ( #7192, #536, #3229 ) ) ;
#10714=FACE_OUTER_BOUND ( 'NONE', #15289, .T. ) ;
#10755=EDGE_CURVE ( 'NONE', #379, #15035, #14211, .T. ) ;
#10776=DIRECTION ( 'NONE',  ( -1.000000000000000000, 0.000000000000000000, 0.000000000000000000 ) ) ;
#10777=CARTESIAN_POINT ( 'NONE',  ( 0.000000000000000000, 6.928203230275487456, 4.000000000000003553 ) ) ;
#10793=APPLICATION_CONTEXT ( 'automotive_design' ) ;
#10810=( GEOMETRIC_REPRESENTATION_CONTEXT ( 3 ) GLOBAL_UNCERTAINTY_ASSIGNED_CONTEXT ( ( #5206 ) ) GLOBAL_UNIT_ASSIGNED_CONTEXT ( ( #5727, #8267, #4453 ) ) REPRESENTATION_CONTEXT ( 'NONE', 'WORKASPACE' ) );
#10876=ORIENTED_EDGE ( 'NONE', *, *, #7793, .F. ) ;
#10880=CARTESIAN_POINT ( 'NONE',  ( 0.3194001229790260354, 3.115132258388565223, -7.999999999999979572 ) ) ;
#10928=DIRECTION ( 'NONE',  ( 0.000000000000000000, 0.000000000000000000, -1.000000000000000000 ) ) ;
#10950=DIRECTION ( 'NONE',  ( 0.000000000000000000, -0.8660254037844379305, 0.5000000000000012212 ) ) ;
#10956=CARTESIAN_POINT ( 'NONE',  ( 5.799999999999999822, 6.928203230275514990, -4.000000000000003553 ) ) ;
#10969=EDGE_CURVE ( 'NONE', #1214, #8453, #2000, .T. ) ;
#10975=EDGE_CURVE ( 'NONE', #5430, #14943, #5319, .T. ) ;
#11002=EDGE_CURVE ( 'NONE', #12934, #3554, #13342, .T. ) ;
#11016=ORIENTED_EDGE ( 'NONE', *, *, #11440, .F. ) ;
#11026=VERTEX_POINT ( 'NONE', #10522 ) ;
#11055=CARTESIAN_POINT ( 'NONE',  ( 5.799999999999999822, 4.618802153516981868, -7.999999999999979572 ) ) ;
#11175=ORIENTED_EDGE ( 'NONE', *, *, #10203, .T. ) ;
#11202=AXIS2_PLACEMENT_3D ( 'NONE', #14898, #13882, #8926 ) ;
#11229=DIRECTION ( 'NONE',  ( -1.000000000000000000, 0.000000000000000000, 0.000000000000000000 ) ) ;
#11265=FACE_OUTER_BOUND ( 'NONE', #14696, .T. ) ;
#11270=DIRECTION ( 'NONE',  ( 0.000000000000000000, -1.000000000000000000, 0.000000000000000000 ) ) ;
#11291=CARTESIAN_POINT ( 'NONE',  ( 5.799999999999999822, -6.928203230275514990, -4.000000000000003553 ) ) ;
#11300=PLANE ( 'NONE',  #6513 ) ;
#11336=VECTOR ( 'NONE', #5484, 999.9999999999998863 ) ;
#11338=LINE ( 'NONE', #3052, #14157 ) ;
#11350=CONICAL_SURFACE ( 'NONE', #2276, 8.000000000000028422, 1.047197551196600296 ) ;
#11382=EDGE_LOOP ( 'NONE', ( #9244, #3001, #7555, #314, #14768, #13737 ) ) ;
#11386=CIRCLE ( 'NONE', #13389, 8.000000000000028422 ) ;
#11428=ORIENTED_EDGE ( 'NONE', *, *, #5465, .T. ) ;
#11435=ADVANCED_FACE ( 'NONE', ( #1232 ), #6170, .T. ) ;
#11440=EDGE_CURVE ( 'NONE', #10266, #4760, #12957, .T. ) ;
#11450=CARTESIAN_POINT ( 'NONE',  ( 0.01688885742777454860, -7.321065037175440438, -3.319543390096036273 ) ) ;
#11457=DIRECTION ( 'NONE',  ( 1.000000000000000000, 0.000000000000000000, 0.000000000000000000 ) ) ;
#11461=EDGE_LOOP ( 'NONE', ( #1536, #9328, #11175, #3911, #4656, #6879 ) ) ;
#11513=CARTESIAN_POINT ( 'NONE',  ( 5.799999999999999822, -4.618802153516981868, 8.000000000000007105 ) ) ;
#11519=FACE_OUTER_BOUND ( 'NONE', #1064, .T. ) ;
#11526=CARTESIAN_POINT ( 'NONE',  ( 6.399999999999999467, 0.000000000000000000, 0.000000000000000000 ) ) ;
#11536=ADVANCED_FACE ( 'NONE', ( #11265 ), #420, .T. ) ;
#11580=FACE_BOUND ( 'NONE', #5886, .T. ) ;
#11630=AXIS2_PLACEMENT_3D ( 'NONE', #8207, #10322, #5505 ) ;
#11635=CARTESIAN_POINT ( 'NONE',  ( 6.399999999999999467, 6.613092715395731132E-16, 5.400000000000019007 ) ) ;
#11639=DIRECTION ( 'NONE',  ( 0.000000000000000000, 0.000000000000000000, -1.000000000000000000 ) ) ;
#11693=PLANE ( 'NONE',  #5879 ) ;
#11705=ORIENTED_EDGE ( 'NONE', *, *, #13012, .F. ) ;
#11711=CARTESIAN_POINT ( 'NONE',  ( 5.799999999999999822, 0.000000000000000000, 8.000000000000007105 ) ) ;
#11736=ORIENTED_EDGE ( 'NONE', *, *, #7900, .T. ) ;
#11743=VECTOR ( 'NONE', #15461, 1000.000000000000000 ) ;
#11747=CARTESIAN_POINT ( 'NONE',  ( 0.000000000000000000, -2.775557561562891351E-14, -8.000000000000007105 ) ) ;
#11768=VECTOR ( 'NONE', #8901, 1000.000000000000000 ) ;
#11773=CARTESIAN_POINT ( 'NONE',  ( 0.4973051450695281650, -3.866309095700691145, 8.000000000000007105 ) ) ;
#11783=DIRECTION ( 'NONE',  ( -1.000000000000000000, 0.000000000000000000, 0.000000000000000000 ) ) ;
#11788=ORIENTED_EDGE ( 'NONE', *, *, #1311, .F. ) ;
#11814=CARTESIAN_POINT ( 'NONE',  ( 5.799999999999999822, 4.618802153516981868, -7.999999999999979572 ) ) ;
#11821=CARTESIAN_POINT ( 'NONE',  ( -1.273212868926705820E-14, 0.3912769056150044999, -7.999999999999981348 ) ) ;
#11860=FACE_OUTER_BOUND ( 'NONE', #10192, .T. ) ;
#11907=DIRECTION ( 'NONE',  ( 1.000000000000000000, 0.000000000000000000, 0.000000000000000000 ) ) ;
#11933=ORIENTED_EDGE ( 'NONE', *, *, #4198, .F. ) ;
#11957=ORIENTED_EDGE ( 'NONE', *, *, #11002, .F. ) ;
#11966=CARTESIAN_POINT ( 'NONE',  ( 0.01688885742775080370, 6.535341423375568226, -4.680456609903959730 ) ) ;
#11981=CARTESIAN_POINT ( 'NONE',  ( 0.4988340113715870050, 3.871605243926933504, 8.000000000000007105 ) ) ;
#12036=ORIENTED_EDGE ( 'NONE', *, *, #12857, .T. ) ;
#12037=FACE_OUTER_BOUND ( 'NONE', #9689, .T. ) ;
#12064=ORIENTED_EDGE ( 'NONE', *, *, #791, .F. ) ;
#12114=DIRECTION ( 'NONE',  ( 0.000000000000000000, 0.000000000000000000, -1.000000000000000000 ) ) ;
#12130=CARTESIAN_POINT ( 'NONE',  ( 0.08285530295199074191, 1.570896314769977931, 8.000000000000007105 ) ) ;
#12243=AXIS2_PLACEMENT_3D ( 'NONE', #2053, #6891, #15301 ) ;
#12288=CARTESIAN_POINT ( 'NONE',  ( 6.800000000000000711, 0.000000000000000000, 0.000000000000000000 ) ) ;
#12291=CARTESIAN_POINT ( 'NONE',  ( 5.799999999999999822, -9.237604307034018802, 2.775557561562891351E-14 ) ) ;
#12302=LINE ( 'NONE', #11055, #6361 ) ;
#12312=AXIS2_PLACEMENT_3D ( 'NONE', #3785, #8530, #12881 ) ;
#12320=ORIENTED_EDGE ( 'NONE', *, *, #6344, .T. ) ;
#12337=AXIS2_PLACEMENT_3D ( 'NONE', #4568, #8147, #5681 ) ;
#12338=EDGE_CURVE ( 'NONE', #14309, #50, #8479, .T. ) ;
#12379=ORIENTED_EDGE ( 'NONE', *, *, #6005, .T. ) ;
#12384=DIRECTION ( 'NONE',  ( 0.000000000000000000, 0.4999999999999996669, -0.8660254037844388186 ) ) ;
#12408=ORIENTED_EDGE ( 'NONE', *, *, #9434, .F. ) ;
#12435=PLANE ( 'NONE',  #14449 ) ;
#12445=ORIENTED_EDGE ( 'NONE', *, *, #2573, .T. ) ;
#12449=CARTESIAN_POINT ( 'NONE',  ( 51.39999999999999858, 0.000000000000000000, 0.000000000000000000 ) ) ;
#12502=ADVANCED_FACE ( 'NONE', ( #5226 ), #8977, .F. ) ;
#12523=PLANE ( 'NONE',  #1847 ) ;
#12562=DIRECTION ( 'NONE',  ( -1.000000000000000000, -0.000000000000000000, -0.000000000000000000 ) ) ;
#12590=AXIS2_PLACEMENT_3D ( 'NONE', #10219, #7704, #8797 ) ;
#12596=ORIENTED_EDGE ( 'NONE', *, *, #14574, .F. ) ;
#12613=AXIS2_PLACEMENT_3D ( 'NONE', #10195, #9013, #3879 ) ;
#12655=ORIENTED_EDGE ( 'NONE', *, *, #8743, .T. ) ;
#12659=VECTOR ( 'NONE', #5864, 999.9999999999997726 ) ;
#12660=( GEOMETRIC_REPRESENTATION_CONTEXT ( 3 ) GLOBAL_UNCERTAINTY_ASSIGNED_CONTEXT ( ( #9128 ) ) GLOBAL_UNIT_ASSIGNED_CONTEXT ( ( #13081, #7113, #13712 ) ) REPRESENTATION_CONTEXT ( 'NONE', 'WORKASPACE' ) );
#12679=EDGE_CURVE ( 'NONE', #1214, #14616, #9335, .T. ) ;
#12684=ADVANCED_FACE ( 'NONE', ( #10511 ), #15385, .F. ) ;
#12714=CARTESIAN_POINT ( 'NONE',  ( 0.000000000000000000, 0.000000000000000000, 0.000000000000000000 ) ) ;
#12715=AXIS2_PLACEMENT_3D ( 'NONE', #10014, #8744, #7725 ) ;
#12757=ADVANCED_FACE ( 'NONE', ( #10669 ), #4172, .F. ) ;
#12790=FACE_OUTER_BOUND ( 'NONE', #7531, .T. ) ;
#12794=CARTESIAN_POINT ( 'NONE',  ( 0.1306530452038150159, -5.952467836904141940, 5.690023276062422752 ) ) ;
#12854=CARTESIAN_POINT ( 'NONE',  ( 0.7145311798163258565, -9.237604307034018802, 2.775557561562891351E-14 ) ) ;
#12857=EDGE_CURVE ( 'NONE', #6660, #4287, #643, .T. ) ;
#12880=CYLINDRICAL_SURFACE ( 'NONE', #223, 8.000000000000028422 ) ;
#12881=DIRECTION ( 'NONE',  ( 0.000000000000000000, 0.000000000000000000, 1.000000000000000000 ) ) ;
#12914=DIRECTION ( 'NONE',  ( 0.000000000000000000, 0.000000000000000000, -1.000000000000000000 ) ) ;
#12916=ORIENTED_EDGE ( 'NONE', *, *, #9924, .F. ) ;
#12934=VERTEX_POINT ( 'NONE', #2030 ) ;
#12937=PRODUCT ( 'hex bolt gradeab_iso_ISO 4014 - M10 x 45 x 26-N', 'hex bolt gradeab_iso_ISO 4014 - M10 x 45 x 26-N', '', ( #381 ) ) ;
#12941=AXIS2_PLACEMENT_3D ( 'NONE', #10645, #4636, #8368 ) ;
#12957=CIRCLE ( 'NONE', #10198, 8.000000000000028422 ) ;
#12976=ORIENTED_EDGE ( 'NONE', *, *, #13378, .T. ) ;
#12978=CARTESIAN_POINT ( 'NONE',  ( 0.4969600502617326776, 4.995646404165254850, -7.347286611336954820 ) ) ;
#12987=DIRECTION ( 'NONE',  ( 1.000000000000000000, 0.000000000000000000, 0.000000000000000000 ) ) ;
#13007=CARTESIAN_POINT ( 'NONE',  ( 6.800000000000000711, 6.123233995736767268E-16, -5.000000000000000000 ) ) ;
#13012=EDGE_CURVE ( 'NONE', #8751, #207, #5888, .T. ) ;
#13020=DIRECTION ( 'NONE',  ( 0.000000000000000000, 0.000000000000000000, 1.000000000000000000 ) ) ;
#13051=CARTESIAN_POINT ( 'NONE',  ( 0.4969600502617518845, 8.860760056385744932, 0.6527133886630305248 ) ) ;
#13058=PLANE ( 'NONE',  #8333 ) ;
#13072=CARTESIAN_POINT ( 'NONE',  ( 0.000000000000000000, 0.000000000000000000, 0.000000000000000000 ) ) ;
#13081=( LENGTH_UNIT ( ) NAMED_UNIT ( * ) SI_UNIT ( .MILLI., .METRE. ) );
#13082=AXIS2_PLACEMENT_3D ( 'NONE', #2324, #3658, #1199 ) ;
#13093=CARTESIAN_POINT ( 'NONE',  ( 0.3157512944565075141, -3.097794232830054728, 8.000000000000008882 ) ) ;
#13105=DIRECTION ( 'NONE',  ( 0.000000000000000000, 0.000000000000000000, 1.000000000000000000 ) ) ;
#13123=LINE ( 'NONE', #2560, #15605 ) ;
#13127=VECTOR ( 'NONE', #1559, 999.9999999999998863 ) ;
#13135=CARTESIAN_POINT ( 'NONE',  ( 6.399999999999999467, -4.618802153516981868, 8.000000000000007105 ) ) ;
#13147=DIRECTION ( 'NONE',  ( -1.000000000000000000, 0.000000000000000000, 0.000000000000000000 ) ) ;
#13148=CARTESIAN_POINT ( 'NONE',  ( 0.06730325657896167602, -1.557442666625575178, -7.999999999999979572 ) ) ;
#13166=FACE_OUTER_BOUND ( 'NONE', #3657, .T. ) ;
#13207=CARTESIAN_POINT ( 'NONE',  ( 0.000000000000000000, 6.928203230275514990, -4.000000000000003553 ) ) ;
#13239=FILL_AREA_STYLE ('',( #2599 ) ) ;
#13240=LINE ( 'NONE', #7497, #1836 ) ;
#13245=AXIS2_PLACEMENT_3D ( 'NONE', #14130, #14361, #3325 ) ;
#13286=AXIS2_PLACEMENT_3D ( 'NONE', #7187, #15358, #7022 ) ;
#13309=PRODUCT_DEFINITION_FORMATION_WITH_SPECIFIED_SOURCE ( 'ANY', '', #12937, .NOT_KNOWN. ) ;
#13314=ORIENTED_EDGE ( 'NONE', *, *, #10370, .T. ) ;
#13342=CIRCLE ( 'NONE', #13856, 5.000000000000017764 ) ;
#13358=ORIENTED_EDGE ( 'NONE', *, *, #10684, .F. ) ;
#13361=DIRECTION ( 'NONE',  ( 0.000000000000000000, 0.000000000000000000, 1.000000000000000000 ) ) ;
#13363=EDGE_CURVE ( 'NONE', #14309, #6660, #2622, .T. ) ;
#13378=EDGE_CURVE ( 'NONE', #2448, #5048, #10199, .T. ) ;
#13385=CARTESIAN_POINT ( 'NONE',  ( 0.01678220609566356131, 0.7854258609844410044, 8.000000000000008882 ) ) ;
#13389=AXIS2_PLACEMENT_3D ( 'NONE', #14736, #14500, #6081 ) ;
#13407=ORIENTED_EDGE ( 'NONE', *, *, #7544, .F. ) ;
#13419=ORIENTED_EDGE ( 'NONE', *, *, #13363, .T. ) ;
#13451=PLANE ( 'NONE',  #10064 ) ;
#13465=ADVANCED_FACE ( 'NONE', ( #1699 ), #12435, .T. ) ;
#13476=LINE ( 'NONE', #12291, #13127 ) ;
#13517=EDGE_CURVE ( 'NONE', #8751, #10266, #8445, .T. ) ;
#13555=CIRCLE ( 'NONE', #12312, 8.000000000000028422 ) ;
#13569=CARTESIAN_POINT ( 'NONE',  ( 0.7145311798161593231, -4.618802153517259867, -7.999999999999979572 ) ) ;
#13602=AXIS2_PLACEMENT_3D ( 'NONE', #5479, #639, #13831 ) ;
#13635=EDGE_LOOP ( 'NONE', ( #12064, #10226, #13984, #8159, #2829, #10876 ) ) ;
#13663=CARTESIAN_POINT ( 'NONE',  ( 6.800000000000000711, 0.000000000000000000, 0.000000000000000000 ) ) ;
#13676=EDGE_CURVE ( 'NONE', #14204, #12934, #4092, .T. ) ;
#13692=ADVANCED_FACE ( 'NONE', ( #7746 ), #2369, .T. ) ;
#13712=( NAMED_UNIT ( * ) SI_UNIT ( $, .STERADIAN. ) SOLID_ANGLE_UNIT ( ) );
#13733=ADVANCED_FACE ( 'NONE', ( #11519 ), #6715, .F. ) ;
#13737=ORIENTED_EDGE ( 'NONE', *, *, #318, .F. ) ;
#13747=EDGE_LOOP ( 'NONE', ( #9895, #4784, #5509, #1408, #13407, #5306 ) ) ;
#13748=CARTESIAN_POINT ( 'NONE',  ( 0.4969600502617546600, -4.995646404165271726, 7.347286611336989459 ) ) ;
#13784=ADVANCED_FACE ( 'NONE', ( #2192 ), #4637, .F. ) ;
#13811=VECTOR ( 'NONE', #14318, 1000.000000000000000 ) ;
#13831=DIRECTION ( 'NONE',  ( 0.000000000000000000, 1.000000000000000000, 0.000000000000000000 ) ) ;
#13856=AXIS2_PLACEMENT_3D ( 'NONE', #1043, #7141, #4672 ) ;
#13879=DIRECTION ( 'NONE',  ( 0.000000000000000000, 0.000000000000000000, -1.000000000000000000 ) ) ;
#13882=DIRECTION ( 'NONE',  ( 1.000000000000000000, 0.000000000000000000, 0.000000000000000000 ) ) ;
#13895=ADVANCED_FACE ( 'NONE', ( #626 ), #11300, .F. ) ;
#13896=CIRCLE ( 'NONE', #265, 4.172000000000013920 ) ;
#13962=DIRECTION ( 'NONE',  ( 0.000000000000000000, 0.8660254037844388186, 0.4999999999999996669 ) ) ;
#13973=CARTESIAN_POINT ( 'NONE',  ( 5.799999999999999822, -9.237604307034018802, 2.775557561562891351E-14 ) ) ;
#13984=ORIENTED_EDGE ( 'NONE', *, *, #13378, .F. ) ;
#14009=FACE_OUTER_BOUND ( 'NONE', #8163, .T. ) ;
#14016=CARTESIAN_POINT ( 'NONE',  ( 6.399999999999999467, 9.237604307034018802, 0.000000000000000000 ) ) ;
#14019=ORIENTED_EDGE ( 'NONE', *, *, #7900, .F. ) ;
#14023=CARTESIAN_POINT ( 'NONE',  ( 5.799999999999999822, -9.237604307034018802, 2.775557561562891351E-14 ) ) ;
#14055=CYLINDRICAL_SURFACE ( 'NONE', #7540, 5.000000000000017764 ) ;
#14057=ORIENTED_EDGE ( 'NONE', *, *, #4687, .T. ) ;
#14069=ORIENTED_EDGE ( 'NONE', *, *, #967, .T. ) ;
#14113=VECTOR ( 'NONE', #1455, 1000.000000000000000 ) ;
#14122=DIRECTION ( 'NONE',  ( 0.000000000000000000, 0.000000000000000000, -1.000000000000000000 ) ) ;
#14130=CARTESIAN_POINT ( 'NONE',  ( 6.399999999999999467, 9.237604307034018802, 0.000000000000000000 ) ) ;
#14134=ORIENTED_EDGE ( 'NONE', *, *, #13363, .F. ) ;
#14135=ORIENTED_EDGE ( 'NONE', *, *, #624, .T. ) ;
#14157=VECTOR ( 'NONE', #14952, 1000.000000000000000 ) ;
#14194=CARTESIAN_POINT ( 'NONE',  ( 0.06809871960542948632, -7.710219529346599820, 2.645508037661917555 ) ) ;
#14204=VERTEX_POINT ( 'NONE', #15362 ) ;
#14211=B_SPLINE_CURVE_WITH_KNOTS ( 'NONE', 3,
 ( #13207, #10703, #11966, #3665, #4616, #2405, #12978, #2247 ),
 .UNSPECIFIED., .F., .F.,
 ( 4, 2, 2, 4 ),
 ( 0.004673709593152154847, 0.005837709341827654677, 0.007001709090503155375, 0.009329708587854153301 ),
 .UNSPECIFIED. ) ;
#14262=CARTESIAN_POINT ( 'NONE',  ( 0.7145311798161593231, -4.618802153517259867, -7.999999999999979572 ) ) ;
#14267=ORIENTED_EDGE ( 'NONE', *, *, #11440, .T. ) ;
#14271=SURFACE_STYLE_USAGE ( .BOTH. , #2438 ) ;
#14276=ORIENTED_EDGE ( 'NONE', *, *, #10488, .F. ) ;
#14279=CARTESIAN_POINT ( 'NONE',  ( 0.7145311798163155315, -4.618802153516981868, 8.000000000000007105 ) ) ;
#14305=CARTESIAN_POINT ( 'NONE',  ( 0.4964154566687909442, 4.996589667937362478, 7.345652830558772273 ) ) ;
#14308=AXIS2_PLACEMENT_3D ( 'NONE', #874, #11783, #13105 ) ;
#14309=VERTEX_POINT ( 'NONE', #8675 ) ;
#14318=DIRECTION ( 'NONE',  ( -1.000000000000000000, 0.000000000000000000, 0.000000000000000000 ) ) ;
#14361=DIRECTION ( 'NONE',  ( 0.000000000000000000, -0.8660254037844380415, -0.5000000000000011102 ) ) ;
#14406=ORIENTED_EDGE ( 'NONE', *, *, #13517, .T. ) ;
#14410=EDGE_CURVE ( 'NONE', #3554, #12934, #9792, .T. ) ;
#14444=DIRECTION ( 'NONE',  ( 1.000000000000000000, 0.000000000000000000, 0.000000000000000000 ) ) ;
#14449=AXIS2_PLACEMENT_3D ( 'NONE', #7643, #113, #2662 ) ;
#14457=LINE ( 'NONE', #1123, #8094 ) ;
#14459=ORIENTED_EDGE ( 'NONE', *, *, #6543, .T. ) ;
#14473=CARTESIAN_POINT ( 'NONE',  ( 0.000000000000000000, 6.928203230275514990, -4.000000000000003553 ) ) ;
#14476=FACE_OUTER_BOUND ( 'NONE', #15365, .T. ) ;
#14483=DIRECTION ( 'NONE',  ( 1.000000000000000000, 0.000000000000000000, 0.000000000000000000 ) ) ;
#14500=DIRECTION ( 'NONE',  ( -1.000000000000000000, 0.000000000000000000, 0.000000000000000000 ) ) ;
#14513=PRODUCT_DEFINITION ( 'UNKNOWN', '', #13309, #1566 ) ;
#14519=DIRECTION ( 'NONE',  ( 0.000000000000000000, -0.5000000000000012212, 0.8660254037844380415 ) ) ;
#14526=VECTOR ( 'NONE', #7658, 1000.000000000000000 ) ;
#14557=AXIS2_PLACEMENT_3D ( 'NONE', #12288, #1712, #193 ) ;
#14570=DIRECTION ( 'NONE',  ( 0.000000000000000000, 0.000000000000000000, -1.000000000000000000 ) ) ;
#14574=EDGE_CURVE ( 'NONE', #14943, #10460, #15263, .T. ) ;
#14594=B_SPLINE_CURVE_WITH_KNOTS ( 'NONE', 3,
 ( #4788, #1379, #13385, #12130, #9854, #7410, #11981, #3846 ),
 .UNSPECIFIED., .F., .F.,
 ( 4, 2, 2, 4 ),
 ( 0.01336725832182607265, 0.01453745201803763321, 0.01570764571424919376, 0.01804803310667231833 ),
 .UNSPECIFIED. ) ;
#14607=AXIS2_PLACEMENT_3D ( 'NONE', #15161, #9193, #3255 ) ;
#14616=VERTEX_POINT ( 'NONE', #2337 ) ;
#14639=VERTEX_POINT ( 'NONE', #11814 ) ;
#14667=CIRCLE ( 'NONE', #1551, 0.4000000000000001887 ) ;
#14673=ORIENTED_EDGE ( 'NONE', *, *, #967, .F. ) ;
#14680=CARTESIAN_POINT ( 'NONE',  ( 0.000000000000000000, 6.928203230275514990, -4.000000000000003553 ) ) ;
#14696=EDGE_LOOP ( 'NONE', ( #4101, #5291, #2317, #2567 ) ) ;
#14701=EDGE_CURVE ( 'NONE', #4918, #8392, #15422, .T. ) ;
#14720=CARTESIAN_POINT ( 'NONE',  ( 6.399999999999999467, -9.237604307034018802, 2.775557561562891351E-14 ) ) ;
#14721=FACE_OUTER_BOUND ( 'NONE', #6796, .T. ) ;
#14735=FACE_OUTER_BOUND ( 'NONE', #3226, .T. ) ;
#14736=CARTESIAN_POINT ( 'NONE',  ( 5.799999999999999822, 0.000000000000000000, 0.000000000000000000 ) ) ;
#14738=FACE_OUTER_BOUND ( 'NONE', #13635, .T. ) ;
#14768=ORIENTED_EDGE ( 'NONE', *, *, #3073, .F. ) ;
#14806=CARTESIAN_POINT ( 'NONE',  ( 5.799999999999999822, -6.928203230275514990, 4.000000000000058620 ) ) ;
#14812=ADVANCED_FACE ( 'NONE', ( #14476 ), #13451, .F. ) ;
#14832=SHAPE_DEFINITION_REPRESENTATION ( #4623, #3387 ) ;
#14849=CARTESIAN_POINT ( 'NONE',  ( 1.960598928577951748E-15, -6.732211846623379792, 4.339467034331228490 ) ) ;
#14856=VECTOR ( 'NONE', #9418, 1000.000000000000000 ) ;
#14898=CARTESIAN_POINT ( 'NONE',  ( 0.000000000000000000, 0.000000000000000000, 0.000000000000000000 ) ) ;
#14928=ORIENTED_EDGE ( 'NONE', *, *, #10755, .T. ) ;
#14937=CARTESIAN_POINT ( 'NONE',  ( 6.399999999999999467, 0.000000000000000000, 0.000000000000000000 ) ) ;
#14943=VERTEX_POINT ( 'NONE', #1688 ) ;
#14952=DIRECTION ( 'NONE',  ( -1.000000000000000000, 0.000000000000000000, 0.000000000000000000 ) ) ;
#14991=ORIENTED_EDGE ( 'NONE', *, *, #12338, .F. ) ;
#15006=CARTESIAN_POINT ( 'NONE',  ( 0.000000000000000000, -6.928203230275514990, 4.000000000000058620 ) ) ;
#15035=VERTEX_POINT ( 'NONE', #2316 ) ;
#15056=CARTESIAN_POINT ( 'NONE',  ( 0.1306530452038175694, -7.903938623646883599, -2.309976723937606113 ) ) ;
#15062=AXIS2_PLACEMENT_3D ( 'NONE', #12449, #6551, #6472 ) ;
#15161=CARTESIAN_POINT ( 'NONE',  ( 6.399999999999999467, -9.237604307034018802, 2.775557561562891351E-14 ) ) ;
#15177=STYLED_ITEM ( 'NONE', ( #6232 ), #243 ) ;
#15217=DIRECTION ( 'NONE',  ( 1.000000000000000000, 0.000000000000000000, 0.000000000000000000 ) ) ;
#15258=SHAPE_REPRESENTATION_RELATIONSHIP ( 'NONE' , 'NONE' ,  #3387, #15616 ) ;
#15263=LINE ( 'NONE', #9520, #13811 ) ;
#15282=DIRECTION ( 'NONE',  ( 0.000000000000000000, -1.000000000000000000, 0.000000000000000000 ) ) ;
#15289=EDGE_LOOP ( 'NONE', ( #1689, #5320, #2197 ) ) ;
#15301=DIRECTION ( 'NONE',  ( 0.000000000000000000, 0.000000000000000000, -1.000000000000000000 ) ) ;
#15308=DIRECTION ( 'NONE',  ( 0.000000000000000000, -1.000000000000000000, 0.000000000000000000 ) ) ;
#15346=ORIENTED_EDGE ( 'NONE', *, *, #6005, .F. ) ;
#15349=ADVANCED_FACE ( 'NONE', ( #6586 ), #2788, .T. ) ;
#15358=DIRECTION ( 'NONE',  ( 1.000000000000000000, 0.000000000000000000, 0.000000000000000000 ) ) ;
#15362=CARTESIAN_POINT ( 'NONE',  ( 51.39999999999999858, 5.616230220889761452E-16, -4.171999999999999709 ) ) ;
#15365=EDGE_LOOP ( 'NONE', ( #14019, #12445, #5422, #6466, #4439, #3892 ) ) ;
#15385=PLANE ( 'NONE',  #13245 ) ;
#15422=LINE ( 'NONE', #13135, #10556 ) ;
#15461=DIRECTION ( 'NONE',  ( -1.000000000000000000, 0.000000000000000000, 0.000000000000000000 ) ) ;
#15506=EDGE_LOOP ( 'NONE', ( #12379, #2685, #12976 ) ) ;
#15508=CARTESIAN_POINT ( 'NONE',  ( 0.01678220609564771287, 0.7854258609844245731, -7.999999999999979572 ) ) ;
#15520=CARTESIAN_POINT ( 'NONE',  ( 6.800000000000000711, 0.000000000000000000, -5.400000000000019007 ) ) ;
#15525=CARTESIAN_POINT ( 'NONE',  ( 0.000000000000000000, -2.775557561562891351E-14, -8.000000000000007105 ) ) ;
#15545=B_SPLINE_CURVE_WITH_KNOTS ( 'NONE', 3,
 ( #15006, #14849, #10286, #1831, #12794, #1982, #13748, #637 ),
 .UNSPECIFIED., .F., .F.,
 ( 4, 2, 2, 4 ),
 ( 0.004673709593152217297, 0.005837709341827692841, 0.007001709090503169253, 0.009329708587854122076 ),
 .UNSPECIFIED. ) ;
#15582=ORIENTED_EDGE ( 'NONE', *, *, #6390, .T. ) ;
#15605=VECTOR ( 'NONE', #10776, 1000.000000000000000 ) ;
#15616=ADVANCED_BREP_SHAPE_REPRESENTATION ( '', ( #243, #12337 ), #10810 ) ;
ENDSEC;
END-ISO-10303-21;
